ISO-10303-21;
HEADER;
/* Generated by software containing ST-Developer
 * from STEP Tools, Inc. (www.steptools.com) 
 */

FILE_DESCRIPTION(
/* description */ (''),
/* implementation_level */ '2;1');

FILE_NAME(
/* name */ 'Plate.step',
/* time_stamp */ '2026-10-22T16:03:28+06:00',
/* author */ (''),
/* organization */ (''),
/* preprocessor_version */ 'ST-DEVELOPER v20.2',
/* originating_system */ 'Autodesk Translation Framework v15.15.0.0',
/* authorisation */ '');

FILE_SCHEMA (('AUTOMOTIVE_DESIGN { 1 0 10303 214 3 1 1 }'));
ENDSEC;

DATA;
#10=MECHANICAL_DESIGN_GEOMETRIC_PRESENTATION_REPRESENTATION('',(#86),#6096);
#64=SHAPE_REPRESENTATION_RELATIONSHIP('SRR','None',#6139,#75);
#75=ADVANCED_BREP_SHAPE_REPRESENTATION('',(#97),#6087);
#86=STYLED_ITEM('',(#6269),#97);
#97=MANIFOLD_SOLID_BREP('Plate',#3595);
#113=FACE_BOUND('',#546,.T.);
#114=FACE_BOUND('',#548,.T.);
#115=FACE_BOUND('',#574,.T.);
#116=FACE_BOUND('',#575,.T.);
#117=FACE_BOUND('',#576,.T.);
#118=FACE_BOUND('',#577,.T.);
#197=PLANE('',#3810);
#198=PLANE('',#3811);
#199=PLANE('',#3812);
#200=PLANE('',#3813);
#201=PLANE('',#3814);
#202=PLANE('',#3815);
#203=PLANE('',#3817);
#204=PLANE('',#3820);
#205=PLANE('',#3823);
#206=PLANE('',#3825);
#207=PLANE('',#3826);
#208=PLANE('',#3827);
#209=PLANE('',#3830);
#210=PLANE('',#3843);
#211=PLANE('',#3844);
#212=PLANE('',#3845);
#213=PLANE('',#3846);
#214=PLANE('',#3847);
#215=PLANE('',#3848);
#216=PLANE('',#3849);
#217=PLANE('',#3850);
#218=PLANE('',#3851);
#219=PLANE('',#3852);
#220=PLANE('',#3853);
#221=PLANE('',#3854);
#222=PLANE('',#3855);
#349=FACE_OUTER_BOUND('',#544,.T.);
#350=FACE_OUTER_BOUND('',#545,.T.);
#351=FACE_OUTER_BOUND('',#547,.T.);
#352=FACE_OUTER_BOUND('',#549,.T.);
#353=FACE_OUTER_BOUND('',#550,.T.);
#354=FACE_OUTER_BOUND('',#551,.T.);
#355=FACE_OUTER_BOUND('',#552,.T.);
#356=FACE_OUTER_BOUND('',#553,.T.);
#357=FACE_OUTER_BOUND('',#554,.T.);
#358=FACE_OUTER_BOUND('',#555,.T.);
#359=FACE_OUTER_BOUND('',#556,.T.);
#360=FACE_OUTER_BOUND('',#557,.T.);
#361=FACE_OUTER_BOUND('',#558,.T.);
#362=FACE_OUTER_BOUND('',#559,.T.);
#363=FACE_OUTER_BOUND('',#560,.T.);
#364=FACE_OUTER_BOUND('',#561,.T.);
#365=FACE_OUTER_BOUND('',#562,.T.);
#366=FACE_OUTER_BOUND('',#563,.T.);
#367=FACE_OUTER_BOUND('',#564,.T.);
#368=FACE_OUTER_BOUND('',#565,.T.);
#369=FACE_OUTER_BOUND('',#566,.T.);
#370=FACE_OUTER_BOUND('',#567,.T.);
#371=FACE_OUTER_BOUND('',#568,.T.);
#372=FACE_OUTER_BOUND('',#569,.T.);
#373=FACE_OUTER_BOUND('',#570,.T.);
#374=FACE_OUTER_BOUND('',#571,.T.);
#375=FACE_OUTER_BOUND('',#572,.T.);
#376=FACE_OUTER_BOUND('',#573,.T.);
#377=FACE_OUTER_BOUND('',#578,.T.);
#378=FACE_OUTER_BOUND('',#579,.T.);
#379=FACE_OUTER_BOUND('',#580,.T.);
#544=EDGE_LOOP('',(#2670,#2671,#2672,#2673));
#545=EDGE_LOOP('',(#2674,#2675,#2676,#2677));
#546=EDGE_LOOP('',(#2678));
#547=EDGE_LOOP('',(#2679,#2680,#2681,#2682));
#548=EDGE_LOOP('',(#2683));
#549=EDGE_LOOP('',(#2684,#2685,#2686,#2687));
#550=EDGE_LOOP('',(#2688,#2689,#2690,#2691));
#551=EDGE_LOOP('',(#2692,#2693,#2694,#2695));
#552=EDGE_LOOP('',(#2696,#2697));
#553=EDGE_LOOP('',(#2698,#2699,#2700));
#554=EDGE_LOOP('',(#2701,#2702,#2703));
#555=EDGE_LOOP('',(#2704,#2705));
#556=EDGE_LOOP('',(#2706,#2707,#2708,#2709,#2710,#2711,#2712,#2713,#2714,
#2715,#2716,#2717));
#557=EDGE_LOOP('',(#2718,#2719,#2720,#2721,#2722,#2723,#2724,#2725,#2726,
#2727,#2728,#2729));
#558=EDGE_LOOP('',(#2730,#2731,#2732,#2733,#2734,#2735,#2736,#2737));
#559=EDGE_LOOP('',(#2738,#2739,#2740,#2741,#2742,#2743,#2744,#2745,#2746,
#2747));
#560=EDGE_LOOP('',(#2748,#2749,#2750,#2751,#2752,#2753));
#561=EDGE_LOOP('',(#2754,#2755,#2756,#2757,#2758,#2759));
#562=EDGE_LOOP('',(#2760,#2761,#2762,#2763,#2764,#2765));
#563=EDGE_LOOP('',(#2766,#2767,#2768,#2769,#2770,#2771));
#564=EDGE_LOOP('',(#2772,#2773,#2774,#2775));
#565=EDGE_LOOP('',(#2776,#2777,#2778,#2779));
#566=EDGE_LOOP('',(#2780,#2781,#2782,#2783));
#567=EDGE_LOOP('',(#2784,#2785,#2786,#2787));
#568=EDGE_LOOP('',(#2788,#2789,#2790,#2791));
#569=EDGE_LOOP('',(#2792,#2793,#2794,#2795,#2796,#2797,#2798,#2799,#2800,
#2801,#2802,#2803,#2804,#2805,#2806,#2807));
#570=EDGE_LOOP('',(#2808,#2809,#2810,#2811));
#571=EDGE_LOOP('',(#2812,#2813,#2814,#2815));
#572=EDGE_LOOP('',(#2816,#2817,#2818,#2819));
#573=EDGE_LOOP('',(#2820,#2821,#2822,#2823));
#574=EDGE_LOOP('',(#2824));
#575=EDGE_LOOP('',(#2825));
#576=EDGE_LOOP('',(#2826));
#577=EDGE_LOOP('',(#2827));
#578=EDGE_LOOP('',(#2828,#2829,#2830,#2831));
#579=EDGE_LOOP('',(#2832,#2833,#2834,#2835));
#580=EDGE_LOOP('',(#2836,#2837,#2838,#2839,#2840,#2841,#2842,#2843,#2844,
#2845,#2846,#2847,#2848,#2849,#2850,#2851));
#838=LINE('',#5345,#1217);
#839=LINE('',#5350,#1218);
#840=LINE('',#5352,#1219);
#841=LINE('',#5354,#1220);
#842=LINE('',#5355,#1221);
#843=LINE('',#5359,#1222);
#844=LINE('',#5361,#1223);
#845=LINE('',#5363,#1224);
#846=LINE('',#5364,#1225);
#847=LINE('',#5366,#1226);
#848=LINE('',#5367,#1227);
#849=LINE('',#5370,#1228);
#850=LINE('',#5372,#1229);
#851=LINE('',#5373,#1230);
#852=LINE('',#5376,#1231);
#853=LINE('',#5378,#1232);
#854=LINE('',#5379,#1233);
#855=LINE('',#5384,#1234);
#856=LINE('',#5391,#1235);
#857=LINE('',#5398,#1236);
#858=LINE('',#5403,#1237);
#859=LINE('',#5406,#1238);
#860=LINE('',#5408,#1239);
#861=LINE('',#5409,#1240);
#862=LINE('',#5410,#1241);
#863=LINE('',#5411,#1242);
#864=LINE('',#5414,#1243);
#865=LINE('',#5415,#1244);
#866=LINE('',#5416,#1245);
#867=LINE('',#5418,#1246);
#868=LINE('',#5419,#1247);
#869=LINE('',#5424,#1248);
#870=LINE('',#5426,#1249);
#871=LINE('',#5427,#1250);
#872=LINE('',#5430,#1251);
#873=LINE('',#5432,#1252);
#874=LINE('',#5433,#1253);
#875=LINE('',#5443,#1254);
#876=LINE('',#5447,#1255);
#877=LINE('',#5451,#1256);
#878=LINE('',#5455,#1257);
#879=LINE('',#5458,#1258);
#880=LINE('',#5460,#1259);
#881=LINE('',#5461,#1260);
#882=LINE('',#5464,#1261);
#883=LINE('',#5466,#1262);
#884=LINE('',#5467,#1263);
#885=LINE('',#5470,#1264);
#886=LINE('',#5472,#1265);
#887=LINE('',#5473,#1266);
#888=LINE('',#5477,#1267);
#889=LINE('',#5479,#1268);
#890=LINE('',#5481,#1269);
#891=LINE('',#5482,#1270);
#892=LINE('',#5484,#1271);
#893=LINE('',#5485,#1272);
#894=LINE('',#5489,#1273);
#895=LINE('',#5491,#1274);
#896=LINE('',#5492,#1275);
#897=LINE('',#5494,#1276);
#898=LINE('',#5496,#1277);
#899=LINE('',#5497,#1278);
#900=LINE('',#5500,#1279);
#901=LINE('',#5501,#1280);
#902=LINE('',#5504,#1281);
#903=LINE('',#5505,#1282);
#904=LINE('',#5508,#1283);
#905=LINE('',#5509,#1284);
#906=LINE('',#5512,#1285);
#907=LINE('',#5513,#1286);
#908=LINE('',#5516,#1287);
#909=LINE('',#5517,#1288);
#910=LINE('',#5519,#1289);
#1217=VECTOR('',#4321,11.);
#1218=VECTOR('',#4326,10.);
#1219=VECTOR('',#4327,10.);
#1220=VECTOR('',#4328,10.);
#1221=VECTOR('',#4329,10.);
#1222=VECTOR('',#4332,10.);
#1223=VECTOR('',#4333,10.);
#1224=VECTOR('',#4334,10.);
#1225=VECTOR('',#4335,10.);
#1226=VECTOR('',#4338,10.);
#1227=VECTOR('',#4339,10.);
#1228=VECTOR('',#4342,10.);
#1229=VECTOR('',#4343,10.);
#1230=VECTOR('',#4344,10.);
#1231=VECTOR('',#4347,10.);
#1232=VECTOR('',#4348,10.);
#1233=VECTOR('',#4349,10.);
#1234=VECTOR('',#4354,10.);
#1235=VECTOR('',#4361,10.);
#1236=VECTOR('',#4368,10.);
#1237=VECTOR('',#4373,10.);
#1238=VECTOR('',#4376,10.);
#1239=VECTOR('',#4377,10.);
#1240=VECTOR('',#4378,10.);
#1241=VECTOR('',#4379,10.);
#1242=VECTOR('',#4380,10.);
#1243=VECTOR('',#4383,10.);
#1244=VECTOR('',#4384,10.);
#1245=VECTOR('',#4385,10.);
#1246=VECTOR('',#4386,10.);
#1247=VECTOR('',#4387,10.);
#1248=VECTOR('',#4394,10.);
#1249=VECTOR('',#4395,10.);
#1250=VECTOR('',#4396,10.);
#1251=VECTOR('',#4399,10.);
#1252=VECTOR('',#4400,10.);
#1253=VECTOR('',#4401,10.);
#1254=VECTOR('',#4414,10.);
#1255=VECTOR('',#4419,10.);
#1256=VECTOR('',#4424,10.);
#1257=VECTOR('',#4429,10.);
#1258=VECTOR('',#4432,10.);
#1259=VECTOR('',#4433,10.);
#1260=VECTOR('',#4434,10.);
#1261=VECTOR('',#4437,10.);
#1262=VECTOR('',#4438,10.);
#1263=VECTOR('',#4439,10.);
#1264=VECTOR('',#4442,10.);
#1265=VECTOR('',#4443,10.);
#1266=VECTOR('',#4444,10.);
#1267=VECTOR('',#4447,10.);
#1268=VECTOR('',#4448,10.);
#1269=VECTOR('',#4449,10.);
#1270=VECTOR('',#4450,10.);
#1271=VECTOR('',#4453,10.);
#1272=VECTOR('',#4454,10.);
#1273=VECTOR('',#4457,10.);
#1274=VECTOR('',#4458,10.);
#1275=VECTOR('',#4459,10.);
#1276=VECTOR('',#4460,10.);
#1277=VECTOR('',#4461,10.);
#1278=VECTOR('',#4462,10.);
#1279=VECTOR('',#4465,10.);
#1280=VECTOR('',#4466,10.);
#1281=VECTOR('',#4469,10.);
#1282=VECTOR('',#4470,10.);
#1283=VECTOR('',#4473,10.);
#1284=VECTOR('',#4474,10.);
#1285=VECTOR('',#4477,10.);
#1286=VECTOR('',#4478,10.);
#1287=VECTOR('',#4481,10.);
#1288=VECTOR('',#4482,10.);
#1289=VECTOR('',#4485,10.);
#1510=CIRCLE('',#3808,11.5112);
#1511=CIRCLE('',#3809,11.5112);
#1512=CIRCLE('',#3816,10.);
#1513=CIRCLE('',#3818,10.);
#1514=CIRCLE('',#3819,10.);
#1515=CIRCLE('',#3821,10.);
#1516=CIRCLE('',#3822,10.);
#1517=CIRCLE('',#3824,10.);
#1518=CIRCLE('',#3828,10.);
#1519=CIRCLE('',#3829,10.);
#1520=CIRCLE('',#3831,10.);
#1521=CIRCLE('',#3832,10.);
#1522=CIRCLE('',#3833,10.);
#1523=CIRCLE('',#3834,10.);
#1524=CIRCLE('',#3836,10.);
#1525=CIRCLE('',#3838,10.);
#1526=CIRCLE('',#3840,10.);
#1527=CIRCLE('',#3842,10.);
#1682=VERTEX_POINT('',#5342);
#1683=VERTEX_POINT('',#5344);
#1684=VERTEX_POINT('',#5348);
#1685=VERTEX_POINT('',#5349);
#1686=VERTEX_POINT('',#5351);
#1687=VERTEX_POINT('',#5353);
#1688=VERTEX_POINT('',#5357);
#1689=VERTEX_POINT('',#5358);
#1690=VERTEX_POINT('',#5360);
#1691=VERTEX_POINT('',#5362);
#1692=VERTEX_POINT('',#5369);
#1693=VERTEX_POINT('',#5371);
#1694=VERTEX_POINT('',#5375);
#1695=VERTEX_POINT('',#5377);
#1696=VERTEX_POINT('',#5381);
#1697=VERTEX_POINT('',#5382);
#1698=VERTEX_POINT('',#5386);
#1699=VERTEX_POINT('',#5387);
#1700=VERTEX_POINT('',#5389);
#1701=VERTEX_POINT('',#5393);
#1702=VERTEX_POINT('',#5394);
#1703=VERTEX_POINT('',#5396);
#1704=VERTEX_POINT('',#5400);
#1705=VERTEX_POINT('',#5401);
#1706=VERTEX_POINT('',#5405);
#1707=VERTEX_POINT('',#5407);
#1708=VERTEX_POINT('',#5413);
#1709=VERTEX_POINT('',#5417);
#1710=VERTEX_POINT('',#5423);
#1711=VERTEX_POINT('',#5425);
#1712=VERTEX_POINT('',#5429);
#1713=VERTEX_POINT('',#5431);
#1714=VERTEX_POINT('',#5434);
#1715=VERTEX_POINT('',#5437);
#1716=VERTEX_POINT('',#5441);
#1717=VERTEX_POINT('',#5445);
#1718=VERTEX_POINT('',#5449);
#1719=VERTEX_POINT('',#5453);
#1720=VERTEX_POINT('',#5457);
#1721=VERTEX_POINT('',#5459);
#1722=VERTEX_POINT('',#5463);
#1723=VERTEX_POINT('',#5465);
#1724=VERTEX_POINT('',#5469);
#1725=VERTEX_POINT('',#5471);
#1726=VERTEX_POINT('',#5475);
#1727=VERTEX_POINT('',#5476);
#1728=VERTEX_POINT('',#5478);
#1729=VERTEX_POINT('',#5480);
#1730=VERTEX_POINT('',#5487);
#1731=VERTEX_POINT('',#5488);
#1732=VERTEX_POINT('',#5490);
#1733=VERTEX_POINT('',#5493);
#1734=VERTEX_POINT('',#5495);
#1735=VERTEX_POINT('',#5499);
#1736=VERTEX_POINT('',#5503);
#1737=VERTEX_POINT('',#5507);
#1738=VERTEX_POINT('',#5511);
#1739=VERTEX_POINT('',#5515);
#2047=EDGE_CURVE('',#1682,#1682,#1510,.T.);
#2048=EDGE_CURVE('',#1682,#1683,#838,.T.);
#2049=EDGE_CURVE('',#1683,#1683,#1511,.T.);
#2050=EDGE_CURVE('',#1684,#1685,#839,.T.);
#2051=EDGE_CURVE('',#1684,#1686,#840,.T.);
#2052=EDGE_CURVE('',#1687,#1686,#841,.T.);
#2053=EDGE_CURVE('',#1685,#1687,#842,.T.);
#2054=EDGE_CURVE('',#1688,#1689,#843,.T.);
#2055=EDGE_CURVE('',#1688,#1690,#844,.T.);
#2056=EDGE_CURVE('',#1691,#1690,#845,.T.);
#2057=EDGE_CURVE('',#1689,#1691,#846,.T.);
#2058=EDGE_CURVE('',#1690,#1687,#847,.T.);
#2059=EDGE_CURVE('',#1686,#1691,#848,.T.);
#2060=EDGE_CURVE('',#1685,#1692,#849,.T.);
#2061=EDGE_CURVE('',#1693,#1692,#850,.T.);
#2062=EDGE_CURVE('',#1684,#1693,#851,.T.);
#2063=EDGE_CURVE('',#1694,#1689,#852,.T.);
#2064=EDGE_CURVE('',#1694,#1695,#853,.T.);
#2065=EDGE_CURVE('',#1695,#1688,#854,.T.);
#2066=EDGE_CURVE('',#1696,#1697,#1512,.T.);
#2067=EDGE_CURVE('',#1697,#1696,#855,.T.);
#2068=EDGE_CURVE('',#1698,#1699,#1513,.T.);
#2069=EDGE_CURVE('',#1699,#1700,#1514,.T.);
#2070=EDGE_CURVE('',#1698,#1700,#856,.T.);
#2071=EDGE_CURVE('',#1701,#1702,#1515,.T.);
#2072=EDGE_CURVE('',#1702,#1703,#1516,.T.);
#2073=EDGE_CURVE('',#1701,#1703,#857,.T.);
#2074=EDGE_CURVE('',#1704,#1705,#1517,.T.);
#2075=EDGE_CURVE('',#1705,#1704,#858,.T.);
#2076=EDGE_CURVE('',#1706,#1694,#859,.T.);
#2077=EDGE_CURVE('',#1707,#1693,#860,.T.);
#2078=EDGE_CURVE('',#1704,#1707,#861,.T.);
#2079=EDGE_CURVE('',#1696,#1705,#862,.T.);
#2080=EDGE_CURVE('',#1706,#1697,#863,.T.);
#2081=EDGE_CURVE('',#1695,#1708,#864,.T.);
#2082=EDGE_CURVE('',#1698,#1708,#865,.T.);
#2083=EDGE_CURVE('',#1701,#1700,#866,.T.);
#2084=EDGE_CURVE('',#1709,#1703,#867,.T.);
#2085=EDGE_CURVE('',#1692,#1709,#868,.T.);
#2086=EDGE_CURVE('',#1703,#1701,#1518,.T.);
#2087=EDGE_CURVE('',#1700,#1698,#1519,.T.);
#2088=EDGE_CURVE('',#1708,#1710,#869,.T.);
#2089=EDGE_CURVE('',#1711,#1710,#870,.T.);
#2090=EDGE_CURVE('',#1711,#1709,#871,.T.);
#2091=EDGE_CURVE('',#1707,#1712,#872,.T.);
#2092=EDGE_CURVE('',#1712,#1713,#873,.T.);
#2093=EDGE_CURVE('',#1713,#1706,#874,.T.);
#2094=EDGE_CURVE('',#1697,#1714,#1520,.T.);
#2095=EDGE_CURVE('',#1714,#1696,#1521,.T.);
#2096=EDGE_CURVE('',#1705,#1715,#1522,.T.);
#2097=EDGE_CURVE('',#1715,#1704,#1523,.T.);
#2098=EDGE_CURVE('',#1716,#1716,#1524,.T.);
#2099=EDGE_CURVE('',#1716,#1702,#875,.T.);
#2100=EDGE_CURVE('',#1717,#1717,#1525,.T.);
#2101=EDGE_CURVE('',#1717,#1715,#876,.T.);
#2102=EDGE_CURVE('',#1718,#1718,#1526,.T.);
#2103=EDGE_CURVE('',#1718,#1699,#877,.T.);
#2104=EDGE_CURVE('',#1719,#1719,#1527,.T.);
#2105=EDGE_CURVE('',#1719,#1714,#878,.T.);
#2106=EDGE_CURVE('',#1711,#1720,#879,.T.);
#2107=EDGE_CURVE('',#1710,#1721,#880,.T.);
#2108=EDGE_CURVE('',#1720,#1721,#881,.T.);
#2109=EDGE_CURVE('',#1720,#1722,#882,.T.);
#2110=EDGE_CURVE('',#1721,#1723,#883,.T.);
#2111=EDGE_CURVE('',#1722,#1723,#884,.T.);
#2112=EDGE_CURVE('',#1722,#1724,#885,.T.);
#2113=EDGE_CURVE('',#1723,#1725,#886,.T.);
#2114=EDGE_CURVE('',#1724,#1725,#887,.T.);
#2115=EDGE_CURVE('',#1726,#1727,#888,.T.);
#2116=EDGE_CURVE('',#1726,#1728,#889,.T.);
#2117=EDGE_CURVE('',#1728,#1729,#890,.T.);
#2118=EDGE_CURVE('',#1727,#1729,#891,.T.);
#2119=EDGE_CURVE('',#1724,#1726,#892,.T.);
#2120=EDGE_CURVE('',#1725,#1728,#893,.T.);
#2121=EDGE_CURVE('',#1730,#1731,#894,.T.);
#2122=EDGE_CURVE('',#1732,#1730,#895,.T.);
#2123=EDGE_CURVE('',#1712,#1732,#896,.T.);
#2124=EDGE_CURVE('',#1727,#1733,#897,.T.);
#2125=EDGE_CURVE('',#1734,#1733,#898,.T.);
#2126=EDGE_CURVE('',#1731,#1734,#899,.T.);
#2127=EDGE_CURVE('',#1732,#1735,#900,.T.);
#2128=EDGE_CURVE('',#1713,#1735,#901,.T.);
#2129=EDGE_CURVE('',#1730,#1736,#902,.T.);
#2130=EDGE_CURVE('',#1735,#1736,#903,.T.);
#2131=EDGE_CURVE('',#1731,#1737,#904,.T.);
#2132=EDGE_CURVE('',#1736,#1737,#905,.T.);
#2133=EDGE_CURVE('',#1738,#1729,#906,.T.);
#2134=EDGE_CURVE('',#1733,#1738,#907,.T.);
#2135=EDGE_CURVE('',#1739,#1738,#908,.T.);
#2136=EDGE_CURVE('',#1734,#1739,#909,.T.);
#2137=EDGE_CURVE('',#1737,#1739,#910,.T.);
#2670=ORIENTED_EDGE('',*,*,#2047,.F.);
#2671=ORIENTED_EDGE('',*,*,#2048,.T.);
#2672=ORIENTED_EDGE('',*,*,#2049,.F.);
#2673=ORIENTED_EDGE('',*,*,#2048,.F.);
#2674=ORIENTED_EDGE('',*,*,#2050,.F.);
#2675=ORIENTED_EDGE('',*,*,#2051,.T.);
#2676=ORIENTED_EDGE('',*,*,#2052,.F.);
#2677=ORIENTED_EDGE('',*,*,#2053,.F.);
#2678=ORIENTED_EDGE('',*,*,#2049,.T.);
#2679=ORIENTED_EDGE('',*,*,#2054,.F.);
#2680=ORIENTED_EDGE('',*,*,#2055,.T.);
#2681=ORIENTED_EDGE('',*,*,#2056,.F.);
#2682=ORIENTED_EDGE('',*,*,#2057,.F.);
#2683=ORIENTED_EDGE('',*,*,#2047,.T.);
#2684=ORIENTED_EDGE('',*,*,#2056,.T.);
#2685=ORIENTED_EDGE('',*,*,#2058,.T.);
#2686=ORIENTED_EDGE('',*,*,#2052,.T.);
#2687=ORIENTED_EDGE('',*,*,#2059,.T.);
#2688=ORIENTED_EDGE('',*,*,#2050,.T.);
#2689=ORIENTED_EDGE('',*,*,#2060,.T.);
#2690=ORIENTED_EDGE('',*,*,#2061,.F.);
#2691=ORIENTED_EDGE('',*,*,#2062,.F.);
#2692=ORIENTED_EDGE('',*,*,#2054,.T.);
#2693=ORIENTED_EDGE('',*,*,#2063,.F.);
#2694=ORIENTED_EDGE('',*,*,#2064,.T.);
#2695=ORIENTED_EDGE('',*,*,#2065,.T.);
#2696=ORIENTED_EDGE('',*,*,#2066,.T.);
#2697=ORIENTED_EDGE('',*,*,#2067,.T.);
#2698=ORIENTED_EDGE('',*,*,#2068,.T.);
#2699=ORIENTED_EDGE('',*,*,#2069,.T.);
#2700=ORIENTED_EDGE('',*,*,#2070,.F.);
#2701=ORIENTED_EDGE('',*,*,#2071,.T.);
#2702=ORIENTED_EDGE('',*,*,#2072,.T.);
#2703=ORIENTED_EDGE('',*,*,#2073,.F.);
#2704=ORIENTED_EDGE('',*,*,#2074,.T.);
#2705=ORIENTED_EDGE('',*,*,#2075,.T.);
#2706=ORIENTED_EDGE('',*,*,#2076,.T.);
#2707=ORIENTED_EDGE('',*,*,#2063,.T.);
#2708=ORIENTED_EDGE('',*,*,#2057,.T.);
#2709=ORIENTED_EDGE('',*,*,#2059,.F.);
#2710=ORIENTED_EDGE('',*,*,#2051,.F.);
#2711=ORIENTED_EDGE('',*,*,#2062,.T.);
#2712=ORIENTED_EDGE('',*,*,#2077,.F.);
#2713=ORIENTED_EDGE('',*,*,#2078,.F.);
#2714=ORIENTED_EDGE('',*,*,#2075,.F.);
#2715=ORIENTED_EDGE('',*,*,#2079,.F.);
#2716=ORIENTED_EDGE('',*,*,#2067,.F.);
#2717=ORIENTED_EDGE('',*,*,#2080,.F.);
#2718=ORIENTED_EDGE('',*,*,#2081,.T.);
#2719=ORIENTED_EDGE('',*,*,#2082,.F.);
#2720=ORIENTED_EDGE('',*,*,#2070,.T.);
#2721=ORIENTED_EDGE('',*,*,#2083,.F.);
#2722=ORIENTED_EDGE('',*,*,#2073,.T.);
#2723=ORIENTED_EDGE('',*,*,#2084,.F.);
#2724=ORIENTED_EDGE('',*,*,#2085,.F.);
#2725=ORIENTED_EDGE('',*,*,#2060,.F.);
#2726=ORIENTED_EDGE('',*,*,#2053,.T.);
#2727=ORIENTED_EDGE('',*,*,#2058,.F.);
#2728=ORIENTED_EDGE('',*,*,#2055,.F.);
#2729=ORIENTED_EDGE('',*,*,#2065,.F.);
#2730=ORIENTED_EDGE('',*,*,#2084,.T.);
#2731=ORIENTED_EDGE('',*,*,#2086,.T.);
#2732=ORIENTED_EDGE('',*,*,#2083,.T.);
#2733=ORIENTED_EDGE('',*,*,#2087,.T.);
#2734=ORIENTED_EDGE('',*,*,#2082,.T.);
#2735=ORIENTED_EDGE('',*,*,#2088,.T.);
#2736=ORIENTED_EDGE('',*,*,#2089,.F.);
#2737=ORIENTED_EDGE('',*,*,#2090,.T.);
#2738=ORIENTED_EDGE('',*,*,#2078,.T.);
#2739=ORIENTED_EDGE('',*,*,#2091,.T.);
#2740=ORIENTED_EDGE('',*,*,#2092,.T.);
#2741=ORIENTED_EDGE('',*,*,#2093,.T.);
#2742=ORIENTED_EDGE('',*,*,#2080,.T.);
#2743=ORIENTED_EDGE('',*,*,#2094,.T.);
#2744=ORIENTED_EDGE('',*,*,#2095,.T.);
#2745=ORIENTED_EDGE('',*,*,#2079,.T.);
#2746=ORIENTED_EDGE('',*,*,#2096,.T.);
#2747=ORIENTED_EDGE('',*,*,#2097,.T.);
#2748=ORIENTED_EDGE('',*,*,#2098,.F.);
#2749=ORIENTED_EDGE('',*,*,#2099,.T.);
#2750=ORIENTED_EDGE('',*,*,#2071,.F.);
#2751=ORIENTED_EDGE('',*,*,#2086,.F.);
#2752=ORIENTED_EDGE('',*,*,#2072,.F.);
#2753=ORIENTED_EDGE('',*,*,#2099,.F.);
#2754=ORIENTED_EDGE('',*,*,#2100,.F.);
#2755=ORIENTED_EDGE('',*,*,#2101,.T.);
#2756=ORIENTED_EDGE('',*,*,#2096,.F.);
#2757=ORIENTED_EDGE('',*,*,#2074,.F.);
#2758=ORIENTED_EDGE('',*,*,#2097,.F.);
#2759=ORIENTED_EDGE('',*,*,#2101,.F.);
#2760=ORIENTED_EDGE('',*,*,#2102,.F.);
#2761=ORIENTED_EDGE('',*,*,#2103,.T.);
#2762=ORIENTED_EDGE('',*,*,#2068,.F.);
#2763=ORIENTED_EDGE('',*,*,#2087,.F.);
#2764=ORIENTED_EDGE('',*,*,#2069,.F.);
#2765=ORIENTED_EDGE('',*,*,#2103,.F.);
#2766=ORIENTED_EDGE('',*,*,#2104,.F.);
#2767=ORIENTED_EDGE('',*,*,#2105,.T.);
#2768=ORIENTED_EDGE('',*,*,#2094,.F.);
#2769=ORIENTED_EDGE('',*,*,#2066,.F.);
#2770=ORIENTED_EDGE('',*,*,#2095,.F.);
#2771=ORIENTED_EDGE('',*,*,#2105,.F.);
#2772=ORIENTED_EDGE('',*,*,#2106,.F.);
#2773=ORIENTED_EDGE('',*,*,#2089,.T.);
#2774=ORIENTED_EDGE('',*,*,#2107,.T.);
#2775=ORIENTED_EDGE('',*,*,#2108,.F.);
#2776=ORIENTED_EDGE('',*,*,#2109,.F.);
#2777=ORIENTED_EDGE('',*,*,#2108,.T.);
#2778=ORIENTED_EDGE('',*,*,#2110,.T.);
#2779=ORIENTED_EDGE('',*,*,#2111,.F.);
#2780=ORIENTED_EDGE('',*,*,#2112,.F.);
#2781=ORIENTED_EDGE('',*,*,#2111,.T.);
#2782=ORIENTED_EDGE('',*,*,#2113,.T.);
#2783=ORIENTED_EDGE('',*,*,#2114,.F.);
#2784=ORIENTED_EDGE('',*,*,#2115,.F.);
#2785=ORIENTED_EDGE('',*,*,#2116,.T.);
#2786=ORIENTED_EDGE('',*,*,#2117,.T.);
#2787=ORIENTED_EDGE('',*,*,#2118,.F.);
#2788=ORIENTED_EDGE('',*,*,#2119,.F.);
#2789=ORIENTED_EDGE('',*,*,#2114,.T.);
#2790=ORIENTED_EDGE('',*,*,#2120,.T.);
#2791=ORIENTED_EDGE('',*,*,#2116,.F.);
#2792=ORIENTED_EDGE('',*,*,#2121,.F.);
#2793=ORIENTED_EDGE('',*,*,#2122,.F.);
#2794=ORIENTED_EDGE('',*,*,#2123,.F.);
#2795=ORIENTED_EDGE('',*,*,#2091,.F.);
#2796=ORIENTED_EDGE('',*,*,#2077,.T.);
#2797=ORIENTED_EDGE('',*,*,#2061,.T.);
#2798=ORIENTED_EDGE('',*,*,#2085,.T.);
#2799=ORIENTED_EDGE('',*,*,#2090,.F.);
#2800=ORIENTED_EDGE('',*,*,#2106,.T.);
#2801=ORIENTED_EDGE('',*,*,#2109,.T.);
#2802=ORIENTED_EDGE('',*,*,#2112,.T.);
#2803=ORIENTED_EDGE('',*,*,#2119,.T.);
#2804=ORIENTED_EDGE('',*,*,#2115,.T.);
#2805=ORIENTED_EDGE('',*,*,#2124,.T.);
#2806=ORIENTED_EDGE('',*,*,#2125,.F.);
#2807=ORIENTED_EDGE('',*,*,#2126,.F.);
#2808=ORIENTED_EDGE('',*,*,#2123,.T.);
#2809=ORIENTED_EDGE('',*,*,#2127,.T.);
#2810=ORIENTED_EDGE('',*,*,#2128,.F.);
#2811=ORIENTED_EDGE('',*,*,#2092,.F.);
#2812=ORIENTED_EDGE('',*,*,#2122,.T.);
#2813=ORIENTED_EDGE('',*,*,#2129,.T.);
#2814=ORIENTED_EDGE('',*,*,#2130,.F.);
#2815=ORIENTED_EDGE('',*,*,#2127,.F.);
#2816=ORIENTED_EDGE('',*,*,#2121,.T.);
#2817=ORIENTED_EDGE('',*,*,#2131,.T.);
#2818=ORIENTED_EDGE('',*,*,#2132,.F.);
#2819=ORIENTED_EDGE('',*,*,#2129,.F.);
#2820=ORIENTED_EDGE('',*,*,#2124,.F.);
#2821=ORIENTED_EDGE('',*,*,#2118,.T.);
#2822=ORIENTED_EDGE('',*,*,#2133,.F.);
#2823=ORIENTED_EDGE('',*,*,#2134,.F.);
#2824=ORIENTED_EDGE('',*,*,#2098,.T.);
#2825=ORIENTED_EDGE('',*,*,#2100,.T.);
#2826=ORIENTED_EDGE('',*,*,#2102,.T.);
#2827=ORIENTED_EDGE('',*,*,#2104,.T.);
#2828=ORIENTED_EDGE('',*,*,#2125,.T.);
#2829=ORIENTED_EDGE('',*,*,#2134,.T.);
#2830=ORIENTED_EDGE('',*,*,#2135,.F.);
#2831=ORIENTED_EDGE('',*,*,#2136,.F.);
#2832=ORIENTED_EDGE('',*,*,#2126,.T.);
#2833=ORIENTED_EDGE('',*,*,#2136,.T.);
#2834=ORIENTED_EDGE('',*,*,#2137,.F.);
#2835=ORIENTED_EDGE('',*,*,#2131,.F.);
#2836=ORIENTED_EDGE('',*,*,#2132,.T.);
#2837=ORIENTED_EDGE('',*,*,#2137,.T.);
#2838=ORIENTED_EDGE('',*,*,#2135,.T.);
#2839=ORIENTED_EDGE('',*,*,#2133,.T.);
#2840=ORIENTED_EDGE('',*,*,#2117,.F.);
#2841=ORIENTED_EDGE('',*,*,#2120,.F.);
#2842=ORIENTED_EDGE('',*,*,#2113,.F.);
#2843=ORIENTED_EDGE('',*,*,#2110,.F.);
#2844=ORIENTED_EDGE('',*,*,#2107,.F.);
#2845=ORIENTED_EDGE('',*,*,#2088,.F.);
#2846=ORIENTED_EDGE('',*,*,#2081,.F.);
#2847=ORIENTED_EDGE('',*,*,#2064,.F.);
#2848=ORIENTED_EDGE('',*,*,#2076,.F.);
#2849=ORIENTED_EDGE('',*,*,#2093,.F.);
#2850=ORIENTED_EDGE('',*,*,#2128,.T.);
#2851=ORIENTED_EDGE('',*,*,#2130,.T.);
#3374=CYLINDRICAL_SURFACE('',#3807,11.5112);
#3375=CYLINDRICAL_SURFACE('',#3835,10.);
#3376=CYLINDRICAL_SURFACE('',#3837,10.);
#3377=CYLINDRICAL_SURFACE('',#3839,10.);
#3378=CYLINDRICAL_SURFACE('',#3841,10.);
#3456=ADVANCED_FACE('',(#349),#3374,.F.);
#3457=ADVANCED_FACE('',(#350,#113),#197,.T.);
#3458=ADVANCED_FACE('',(#351,#114),#198,.T.);
#3459=ADVANCED_FACE('',(#352),#199,.T.);
#3460=ADVANCED_FACE('',(#353),#200,.T.);
#3461=ADVANCED_FACE('',(#354),#201,.T.);
#3462=ADVANCED_FACE('',(#355),#202,.T.);
#3463=ADVANCED_FACE('',(#356),#203,.T.);
#3464=ADVANCED_FACE('',(#357),#204,.T.);
#3465=ADVANCED_FACE('',(#358),#205,.T.);
#3466=ADVANCED_FACE('',(#359),#206,.T.);
#3467=ADVANCED_FACE('',(#360),#207,.T.);
#3468=ADVANCED_FACE('',(#361),#208,.T.);
#3469=ADVANCED_FACE('',(#362),#209,.T.);
#3470=ADVANCED_FACE('',(#363),#3375,.F.);
#3471=ADVANCED_FACE('',(#364),#3376,.F.);
#3472=ADVANCED_FACE('',(#365),#3377,.F.);
#3473=ADVANCED_FACE('',(#366),#3378,.F.);
#3474=ADVANCED_FACE('',(#367),#210,.F.);
#3475=ADVANCED_FACE('',(#368),#211,.F.);
#3476=ADVANCED_FACE('',(#369),#212,.F.);
#3477=ADVANCED_FACE('',(#370),#213,.F.);
#3478=ADVANCED_FACE('',(#371),#214,.F.);
#3479=ADVANCED_FACE('',(#372),#215,.F.);
#3480=ADVANCED_FACE('',(#373),#216,.T.);
#3481=ADVANCED_FACE('',(#374),#217,.T.);
#3482=ADVANCED_FACE('',(#375),#218,.T.);
#3483=ADVANCED_FACE('',(#376,#115,#116,#117,#118),#219,.T.);
#3484=ADVANCED_FACE('',(#377),#220,.T.);
#3485=ADVANCED_FACE('',(#378),#221,.T.);
#3486=ADVANCED_FACE('',(#379),#222,.T.);
#3595=CLOSED_SHELL('',(#3456,#3457,#3458,#3459,#3460,#3461,#3462,#3463,
#3464,#3465,#3466,#3467,#3468,#3469,#3470,#3471,#3472,#3473,#3474,#3475,
#3476,#3477,#3478,#3479,#3480,#3481,#3482,#3483,#3484,#3485,#3486));
#3806=AXIS2_PLACEMENT_3D('',#5340,#4315,#4316);
#3807=AXIS2_PLACEMENT_3D('',#5341,#4317,#4318);
#3808=AXIS2_PLACEMENT_3D('',#5343,#4319,#4320);
#3809=AXIS2_PLACEMENT_3D('',#5346,#4322,#4323);
#3810=AXIS2_PLACEMENT_3D('',#5347,#4324,#4325);
#3811=AXIS2_PLACEMENT_3D('',#5356,#4330,#4331);
#3812=AXIS2_PLACEMENT_3D('',#5365,#4336,#4337);
#3813=AXIS2_PLACEMENT_3D('',#5368,#4340,#4341);
#3814=AXIS2_PLACEMENT_3D('',#5374,#4345,#4346);
#3815=AXIS2_PLACEMENT_3D('',#5380,#4350,#4351);
#3816=AXIS2_PLACEMENT_3D('',#5383,#4352,#4353);
#3817=AXIS2_PLACEMENT_3D('',#5385,#4355,#4356);
#3818=AXIS2_PLACEMENT_3D('',#5388,#4357,#4358);
#3819=AXIS2_PLACEMENT_3D('',#5390,#4359,#4360);
#3820=AXIS2_PLACEMENT_3D('',#5392,#4362,#4363);
#3821=AXIS2_PLACEMENT_3D('',#5395,#4364,#4365);
#3822=AXIS2_PLACEMENT_3D('',#5397,#4366,#4367);
#3823=AXIS2_PLACEMENT_3D('',#5399,#4369,#4370);
#3824=AXIS2_PLACEMENT_3D('',#5402,#4371,#4372);
#3825=AXIS2_PLACEMENT_3D('',#5404,#4374,#4375);
#3826=AXIS2_PLACEMENT_3D('',#5412,#4381,#4382);
#3827=AXIS2_PLACEMENT_3D('',#5420,#4388,#4389);
#3828=AXIS2_PLACEMENT_3D('',#5421,#4390,#4391);
#3829=AXIS2_PLACEMENT_3D('',#5422,#4392,#4393);
#3830=AXIS2_PLACEMENT_3D('',#5428,#4397,#4398);
#3831=AXIS2_PLACEMENT_3D('',#5435,#4402,#4403);
#3832=AXIS2_PLACEMENT_3D('',#5436,#4404,#4405);
#3833=AXIS2_PLACEMENT_3D('',#5438,#4406,#4407);
#3834=AXIS2_PLACEMENT_3D('',#5439,#4408,#4409);
#3835=AXIS2_PLACEMENT_3D('',#5440,#4410,#4411);
#3836=AXIS2_PLACEMENT_3D('',#5442,#4412,#4413);
#3837=AXIS2_PLACEMENT_3D('',#5444,#4415,#4416);
#3838=AXIS2_PLACEMENT_3D('',#5446,#4417,#4418);
#3839=AXIS2_PLACEMENT_3D('',#5448,#4420,#4421);
#3840=AXIS2_PLACEMENT_3D('',#5450,#4422,#4423);
#3841=AXIS2_PLACEMENT_3D('',#5452,#4425,#4426);
#3842=AXIS2_PLACEMENT_3D('',#5454,#4427,#4428);
#3843=AXIS2_PLACEMENT_3D('',#5456,#4430,#4431);
#3844=AXIS2_PLACEMENT_3D('',#5462,#4435,#4436);
#3845=AXIS2_PLACEMENT_3D('',#5468,#4440,#4441);
#3846=AXIS2_PLACEMENT_3D('',#5474,#4445,#4446);
#3847=AXIS2_PLACEMENT_3D('',#5483,#4451,#4452);
#3848=AXIS2_PLACEMENT_3D('',#5486,#4455,#4456);
#3849=AXIS2_PLACEMENT_3D('',#5498,#4463,#4464);
#3850=AXIS2_PLACEMENT_3D('',#5502,#4467,#4468);
#3851=AXIS2_PLACEMENT_3D('',#5506,#4471,#4472);
#3852=AXIS2_PLACEMENT_3D('',#5510,#4475,#4476);
#3853=AXIS2_PLACEMENT_3D('',#5514,#4479,#4480);
#3854=AXIS2_PLACEMENT_3D('',#5518,#4483,#4484);
#3855=AXIS2_PLACEMENT_3D('',#5520,#4486,#4487);
#4315=DIRECTION('axis',(0.,0.,1.));
#4316=DIRECTION('refdir',(1.,0.,0.));
#4317=DIRECTION('center_axis',(0.,1.,0.));
#4318=DIRECTION('ref_axis',(1.,0.,0.));
#4319=DIRECTION('center_axis',(0.,1.,0.));
#4320=DIRECTION('ref_axis',(1.,0.,0.));
#4321=DIRECTION('',(0.,1.,0.));
#4322=DIRECTION('center_axis',(0.,-1.,0.));
#4323=DIRECTION('ref_axis',(1.,0.,0.));
#4324=DIRECTION('center_axis',(0.,1.,0.));
#4325=DIRECTION('ref_axis',(1.,0.,0.));
#4326=DIRECTION('',(-1.,0.,0.));
#4327=DIRECTION('',(0.,0.,-1.));
#4328=DIRECTION('',(1.,0.,0.));
#4329=DIRECTION('',(0.,0.,-1.));
#4330=DIRECTION('center_axis',(0.,-1.,0.));
#4331=DIRECTION('ref_axis',(-1.,0.,0.));
#4332=DIRECTION('',(1.,0.,0.));
#4333=DIRECTION('',(0.,0.,-1.));
#4334=DIRECTION('',(-1.,0.,0.));
#4335=DIRECTION('',(0.,0.,-1.));
#4336=DIRECTION('center_axis',(0.,0.,-1.));
#4337=DIRECTION('ref_axis',(-1.,0.,0.));
#4338=DIRECTION('',(0.,1.,0.));
#4339=DIRECTION('',(0.,-1.,0.));
#4340=DIRECTION('center_axis',(0.,0.,-1.));
#4341=DIRECTION('ref_axis',(-1.,0.,0.));
#4342=DIRECTION('',(0.,1.,0.));
#4343=DIRECTION('',(-1.,0.,0.));
#4344=DIRECTION('',(0.,1.,0.));
#4345=DIRECTION('center_axis',(0.,0.,-1.));
#4346=DIRECTION('ref_axis',(-1.,0.,0.));
#4347=DIRECTION('',(0.,1.,0.));
#4348=DIRECTION('',(-1.,0.,0.));
#4349=DIRECTION('',(0.,1.,0.));
#4350=DIRECTION('center_axis',(0.,0.,1.));
#4351=DIRECTION('ref_axis',(1.,0.,0.));
#4352=DIRECTION('center_axis',(0.,0.,1.));
#4353=DIRECTION('ref_axis',(-1.,0.,0.));
#4354=DIRECTION('',(0.,1.,0.));
#4355=DIRECTION('center_axis',(0.,0.,1.));
#4356=DIRECTION('ref_axis',(1.,0.,0.));
#4357=DIRECTION('center_axis',(0.,0.,1.));
#4358=DIRECTION('ref_axis',(-1.,0.,0.));
#4359=DIRECTION('center_axis',(0.,0.,1.));
#4360=DIRECTION('ref_axis',(-1.,0.,0.));
#4361=DIRECTION('',(0.,1.,0.));
#4362=DIRECTION('center_axis',(0.,0.,1.));
#4363=DIRECTION('ref_axis',(1.,0.,0.));
#4364=DIRECTION('center_axis',(0.,0.,1.));
#4365=DIRECTION('ref_axis',(-1.,0.,0.));
#4366=DIRECTION('center_axis',(0.,0.,1.));
#4367=DIRECTION('ref_axis',(-1.,0.,0.));
#4368=DIRECTION('',(0.,1.,0.));
#4369=DIRECTION('center_axis',(0.,0.,1.));
#4370=DIRECTION('ref_axis',(1.,0.,0.));
#4371=DIRECTION('center_axis',(0.,0.,1.));
#4372=DIRECTION('ref_axis',(-1.,0.,0.));
#4373=DIRECTION('',(0.,1.,0.));
#4374=DIRECTION('center_axis',(1.,0.,0.));
#4375=DIRECTION('ref_axis',(0.,0.,-1.));
#4376=DIRECTION('',(0.,0.,-1.));
#4377=DIRECTION('',(0.,0.,-1.));
#4378=DIRECTION('',(0.,1.,0.));
#4379=DIRECTION('',(0.,1.,0.));
#4380=DIRECTION('',(0.,1.,0.));
#4381=DIRECTION('center_axis',(-1.,0.,0.));
#4382=DIRECTION('ref_axis',(0.,0.,1.));
#4383=DIRECTION('',(0.,0.,1.));
#4384=DIRECTION('',(0.,-1.,0.));
#4385=DIRECTION('',(0.,-1.,0.));
#4386=DIRECTION('',(0.,-1.,0.));
#4387=DIRECTION('',(0.,0.,1.));
#4388=DIRECTION('center_axis',(0.,0.,-1.));
#4389=DIRECTION('ref_axis',(1.,0.,0.));
#4390=DIRECTION('center_axis',(0.,0.,1.));
#4391=DIRECTION('ref_axis',(-1.,0.,0.));
#4392=DIRECTION('center_axis',(0.,0.,1.));
#4393=DIRECTION('ref_axis',(-1.,0.,0.));
#4394=DIRECTION('',(-1.,0.,-8.88178419700125E-17));
#4395=DIRECTION('',(0.,-1.,0.));
#4396=DIRECTION('',(1.,0.,0.));
#4397=DIRECTION('center_axis',(0.,0.,-1.));
#4398=DIRECTION('ref_axis',(1.,0.,0.));
#4399=DIRECTION('',(1.,0.,0.));
#4400=DIRECTION('',(0.,-1.,0.));
#4401=DIRECTION('',(-1.,0.,-8.88178419700125E-17));
#4402=DIRECTION('center_axis',(0.,0.,1.));
#4403=DIRECTION('ref_axis',(-1.,0.,0.));
#4404=DIRECTION('center_axis',(0.,0.,1.));
#4405=DIRECTION('ref_axis',(-1.,0.,0.));
#4406=DIRECTION('center_axis',(0.,0.,1.));
#4407=DIRECTION('ref_axis',(-1.,0.,0.));
#4408=DIRECTION('center_axis',(0.,0.,1.));
#4409=DIRECTION('ref_axis',(-1.,0.,0.));
#4410=DIRECTION('center_axis',(0.,0.,-1.));
#4411=DIRECTION('ref_axis',(-1.,0.,0.));
#4412=DIRECTION('center_axis',(0.,0.,-1.));
#4413=DIRECTION('ref_axis',(-1.,0.,0.));
#4414=DIRECTION('',(0.,0.,-1.));
#4415=DIRECTION('center_axis',(0.,0.,-1.));
#4416=DIRECTION('ref_axis',(-1.,0.,0.));
#4417=DIRECTION('center_axis',(0.,0.,-1.));
#4418=DIRECTION('ref_axis',(-1.,0.,0.));
#4419=DIRECTION('',(0.,0.,-1.));
#4420=DIRECTION('center_axis',(0.,0.,-1.));
#4421=DIRECTION('ref_axis',(-1.,0.,0.));
#4422=DIRECTION('center_axis',(0.,0.,-1.));
#4423=DIRECTION('ref_axis',(-1.,0.,0.));
#4424=DIRECTION('',(0.,0.,-1.));
#4425=DIRECTION('center_axis',(0.,0.,-1.));
#4426=DIRECTION('ref_axis',(-1.,0.,0.));
#4427=DIRECTION('center_axis',(0.,0.,-1.));
#4428=DIRECTION('ref_axis',(-1.,0.,0.));
#4429=DIRECTION('',(0.,0.,-1.));
#4430=DIRECTION('center_axis',(-1.,0.,-8.88178419700125E-17));
#4431=DIRECTION('ref_axis',(8.88178419700125E-17,0.,-1.));
#4432=DIRECTION('',(8.88178419700125E-17,0.,-1.));
#4433=DIRECTION('',(8.88178419700125E-17,0.,-1.));
#4434=DIRECTION('',(0.,-1.,0.));
#4435=DIRECTION('center_axis',(8.88178419700125E-17,0.,-1.));
#4436=DIRECTION('ref_axis',(1.,0.,8.88178419700125E-17));
#4437=DIRECTION('',(1.,0.,8.88178419700125E-17));
#4438=DIRECTION('',(1.,0.,8.88178419700125E-17));
#4439=DIRECTION('',(0.,-1.,0.));
#4440=DIRECTION('center_axis',(-1.,0.,-8.88178419700125E-17));
#4441=DIRECTION('ref_axis',(8.88178419700125E-17,0.,-1.));
#4442=DIRECTION('',(8.88178419700125E-17,0.,-1.));
#4443=DIRECTION('',(8.88178419700125E-17,0.,-1.));
#4444=DIRECTION('',(0.,-1.,0.));
#4445=DIRECTION('center_axis',(1.,0.,8.88178419700125E-17));
#4446=DIRECTION('ref_axis',(-8.88178419700125E-17,0.,1.));
#4447=DIRECTION('',(-8.88178419700125E-17,0.,1.));
#4448=DIRECTION('',(0.,-1.,0.));
#4449=DIRECTION('',(-8.88178419700125E-17,0.,1.));
#4450=DIRECTION('',(0.,-1.,0.));
#4451=DIRECTION('center_axis',(-8.88178419700125E-17,0.,1.));
#4452=DIRECTION('ref_axis',(-1.,0.,-8.88178419700125E-17));
#4453=DIRECTION('',(-1.,0.,-8.88178419700125E-17));
#4454=DIRECTION('',(-1.,0.,-8.88178419700125E-17));
#4455=DIRECTION('center_axis',(0.,-1.,0.));
#4456=DIRECTION('ref_axis',(0.,0.,-1.));
#4457=DIRECTION('',(0.,0.,-1.));
#4458=DIRECTION('',(-1.,0.,0.));
#4459=DIRECTION('',(0.,0.,-1.));
#4460=DIRECTION('',(1.,0.,8.88178419700125E-17));
#4461=DIRECTION('',(0.,0.,1.));
#4462=DIRECTION('',(1.,0.,0.));
#4463=DIRECTION('center_axis',(-1.,0.,0.));
#4464=DIRECTION('ref_axis',(0.,0.,-1.));
#4465=DIRECTION('',(0.,-1.,0.));
#4466=DIRECTION('',(0.,0.,-1.));
#4467=DIRECTION('center_axis',(0.,0.,1.));
#4468=DIRECTION('ref_axis',(-1.,0.,0.));
#4469=DIRECTION('',(0.,-1.,0.));
#4470=DIRECTION('',(-1.,0.,0.));
#4471=DIRECTION('center_axis',(-1.,0.,0.));
#4472=DIRECTION('ref_axis',(0.,0.,-1.));
#4473=DIRECTION('',(0.,-1.,0.));
#4474=DIRECTION('',(0.,0.,-1.));
#4475=DIRECTION('center_axis',(0.,0.,1.));
#4476=DIRECTION('ref_axis',(-1.,0.,0.));
#4477=DIRECTION('',(-1.,0.,0.));
#4478=DIRECTION('',(0.,-1.,0.));
#4479=DIRECTION('center_axis',(1.,0.,0.));
#4480=DIRECTION('ref_axis',(0.,0.,1.));
#4481=DIRECTION('',(0.,0.,1.));
#4482=DIRECTION('',(0.,-1.,0.));
#4483=DIRECTION('center_axis',(0.,0.,-1.));
#4484=DIRECTION('ref_axis',(1.,0.,0.));
#4485=DIRECTION('',(1.,0.,0.));
#4486=DIRECTION('center_axis',(0.,-1.,0.));
#4487=DIRECTION('ref_axis',(0.,0.,-1.));
#5340=CARTESIAN_POINT('',(0.,0.,0.));
#5341=CARTESIAN_POINT('Origin',(4.44089209850063E-15,36.9999821858522,41.5000000000007));
#5342=CARTESIAN_POINT('',(-11.5112,343.,41.5000000000007));
#5343=CARTESIAN_POINT('Origin',(4.44089209850063E-15,343.,41.5000000000007));
#5344=CARTESIAN_POINT('',(-11.5112,363.,41.5000000000007));
#5345=CARTESIAN_POINT('',(-11.5112,36.9999821858522,41.5000000000007));
#5346=CARTESIAN_POINT('Origin',(4.44089209850063E-15,363.,41.5000000000007));
#5347=CARTESIAN_POINT('Origin',(-31.5061608111161,363.,85.0000000000015));
#5348=CARTESIAN_POINT('',(31.5058391888839,363.,85.0000000000015));
#5349=CARTESIAN_POINT('',(-31.5061608111161,363.,85.0000000000015));
#5350=CARTESIAN_POINT('',(-0.000160811116123316,363.,85.0000000000015));
#5351=CARTESIAN_POINT('',(31.5058391888839,363.,25.0000000000015));
#5352=CARTESIAN_POINT('',(31.5058391888839,363.,85.0000000000015));
#5353=CARTESIAN_POINT('',(-31.5061608111161,363.,25.0000000000015));
#5354=CARTESIAN_POINT('',(31.5058391888839,363.,25.0000000000015));
#5355=CARTESIAN_POINT('',(-31.5061608111161,363.,85.0000000000015));
#5356=CARTESIAN_POINT('Origin',(31.5058391888839,343.,85.0000000000015));
#5357=CARTESIAN_POINT('',(-31.5061608111161,343.,85.0000000000015));
#5358=CARTESIAN_POINT('',(31.5058391888839,343.,85.0000000000015));
#5359=CARTESIAN_POINT('',(31.5058391888839,343.,85.0000000000015));
#5360=CARTESIAN_POINT('',(-31.5061608111161,343.,25.0000000000015));
#5361=CARTESIAN_POINT('',(-31.5061608111161,343.,85.0000000000015));
#5362=CARTESIAN_POINT('',(31.5058391888839,343.,25.0000000000015));
#5363=CARTESIAN_POINT('',(-31.5061608111161,343.,25.0000000000015));
#5364=CARTESIAN_POINT('',(31.5058391888839,343.,85.0000000000015));
#5365=CARTESIAN_POINT('Origin',(-0.000160811116125537,353.,25.0000000000015));
#5366=CARTESIAN_POINT('',(-31.5061608111161,363.,25.0000000000015));
#5367=CARTESIAN_POINT('',(31.5058391888839,343.,25.0000000000015));
#5368=CARTESIAN_POINT('Origin',(31.5058391888839,245.5,85.0000000000015));
#5369=CARTESIAN_POINT('',(-31.5061608111161,460.5,85.0000000000015));
#5370=CARTESIAN_POINT('',(-31.5061608111161,245.5,85.0000000000015));
#5371=CARTESIAN_POINT('',(31.5058391888839,460.5,85.0000000000015));
#5372=CARTESIAN_POINT('',(31.5058391888839,460.5,85.0000000000015));
#5373=CARTESIAN_POINT('',(31.5058391888839,245.5,85.0000000000015));
#5374=CARTESIAN_POINT('Origin',(31.5058391888839,245.5,85.0000000000015));
#5375=CARTESIAN_POINT('',(31.5058391888839,245.5,85.0000000000015));
#5376=CARTESIAN_POINT('',(31.5058391888839,245.5,85.0000000000015));
#5377=CARTESIAN_POINT('',(-31.5061608111161,245.5,85.0000000000015));
#5378=CARTESIAN_POINT('',(31.5058391888839,245.5,85.0000000000015));
#5379=CARTESIAN_POINT('',(-31.5061608111161,245.5,85.0000000000015));
#5380=CARTESIAN_POINT('Origin',(-31.5061608111161,245.5,105.000000000001));
#5381=CARTESIAN_POINT('',(31.5058391888839,336.294725687261,105.000000000001));
#5382=CARTESIAN_POINT('',(31.5058391888839,330.773057370623,105.000000000001));
#5383=CARTESIAN_POINT('Origin',(21.8945024061954,333.533891528942,105.000000000001));
#5384=CARTESIAN_POINT('',(31.5058391888839,245.5,105.000000000001));
#5385=CARTESIAN_POINT('Origin',(-31.5061608111161,245.5,105.000000000001));
#5386=CARTESIAN_POINT('',(-31.5061608111161,330.774177285199,105.000000000001));
#5387=CARTESIAN_POINT('',(-11.8945024061954,333.533891528942,105.000000000001));
#5388=CARTESIAN_POINT('Origin',(-21.8945024061954,333.533891528942,105.000000000001));
#5389=CARTESIAN_POINT('',(-31.5061608111161,336.293605772685,105.000000000001));
#5390=CARTESIAN_POINT('Origin',(-21.8945024061954,333.533891528942,105.000000000001));
#5391=CARTESIAN_POINT('',(-31.5061608111161,245.5,105.000000000001));
#5392=CARTESIAN_POINT('Origin',(-31.5061608111161,245.5,105.000000000001));
#5393=CARTESIAN_POINT('',(-31.5061608111161,370.774177285199,105.000000000001));
#5394=CARTESIAN_POINT('',(-11.8945024061954,373.533891528942,105.000000000001));
#5395=CARTESIAN_POINT('Origin',(-21.8945024061954,373.533891528942,105.000000000001));
#5396=CARTESIAN_POINT('',(-31.5061608111161,376.293605772685,105.000000000001));
#5397=CARTESIAN_POINT('Origin',(-21.8945024061954,373.533891528942,105.000000000001));
#5398=CARTESIAN_POINT('',(-31.5061608111161,245.5,105.000000000001));
#5399=CARTESIAN_POINT('Origin',(-31.5061608111161,245.5,105.000000000001));
#5400=CARTESIAN_POINT('',(31.5058391888839,376.294725687261,105.000000000001));
#5401=CARTESIAN_POINT('',(31.5058391888839,370.773057370623,105.000000000001));
#5402=CARTESIAN_POINT('Origin',(21.8945024061954,373.533891528942,105.000000000001));
#5403=CARTESIAN_POINT('',(31.5058391888839,245.5,105.000000000001));
#5404=CARTESIAN_POINT('Origin',(31.5058391888839,245.5,105.000000000001));
#5405=CARTESIAN_POINT('',(31.5058391888839,245.5,105.000000000001));
#5406=CARTESIAN_POINT('',(31.5058391888839,245.5,105.000000000001));
#5407=CARTESIAN_POINT('',(31.5058391888839,460.5,105.000000000001));
#5408=CARTESIAN_POINT('',(31.5058391888839,460.5,105.000000000001));
#5409=CARTESIAN_POINT('',(31.5058391888839,365.5,105.000000000001));
#5410=CARTESIAN_POINT('',(31.5058391888839,365.5,105.000000000001));
#5411=CARTESIAN_POINT('',(31.5058391888839,365.5,105.000000000001));
#5412=CARTESIAN_POINT('Origin',(-31.5061608111161,245.5,85.0000000000015));
#5413=CARTESIAN_POINT('',(-31.5061608111161,245.5,105.000000000001));
#5414=CARTESIAN_POINT('',(-31.5061608111161,245.5,85.0000000000015));
#5415=CARTESIAN_POINT('',(-31.5061608111161,365.5,105.000000000001));
#5416=CARTESIAN_POINT('',(-31.5061608111161,365.5,105.000000000001));
#5417=CARTESIAN_POINT('',(-31.5061608111161,460.5,105.000000000001));
#5418=CARTESIAN_POINT('',(-31.5061608111161,365.5,105.000000000001));
#5419=CARTESIAN_POINT('',(-31.5061608111161,460.5,85.0000000000015));
#5420=CARTESIAN_POINT('Origin',(0.,485.5,105.000000000001));
#5421=CARTESIAN_POINT('Origin',(-21.8945024061954,373.533891528942,105.000000000001));
#5422=CARTESIAN_POINT('Origin',(-21.8945024061954,333.533891528942,105.000000000001));
#5423=CARTESIAN_POINT('',(-67.5061608111161,245.5,105.000000000001));
#5424=CARTESIAN_POINT('',(67.5061608111161,245.5,105.000000000001));
#5425=CARTESIAN_POINT('',(-67.5061608111161,460.5,105.000000000001));
#5426=CARTESIAN_POINT('',(-67.5061608111161,485.5,105.000000000001));
#5427=CARTESIAN_POINT('',(20.626540202779,460.5,105.000000000001));
#5428=CARTESIAN_POINT('Origin',(0.,485.5,105.000000000001));
#5429=CARTESIAN_POINT('',(67.5061608111161,460.5,105.000000000001));
#5430=CARTESIAN_POINT('',(20.626540202779,460.5,105.000000000001));
#5431=CARTESIAN_POINT('',(67.5061608111161,245.5,105.000000000001));
#5432=CARTESIAN_POINT('',(67.5061608111161,485.5,105.000000000001));
#5433=CARTESIAN_POINT('',(67.5061608111161,245.5,105.000000000001));
#5434=CARTESIAN_POINT('',(31.8945024061955,333.533891528942,105.000000000001));
#5435=CARTESIAN_POINT('Origin',(21.8945024061954,333.533891528942,105.000000000001));
#5436=CARTESIAN_POINT('Origin',(21.8945024061954,333.533891528942,105.000000000001));
#5437=CARTESIAN_POINT('',(31.8945024061955,373.533891528942,105.000000000001));
#5438=CARTESIAN_POINT('Origin',(21.8945024061954,373.533891528942,105.000000000001));
#5439=CARTESIAN_POINT('Origin',(21.8945024061954,373.533891528942,105.000000000001));
#5440=CARTESIAN_POINT('Origin',(-21.8945024061954,373.533891528942,120.000000000001));
#5441=CARTESIAN_POINT('',(-11.8945024061954,373.533891528942,120.000000000001));
#5442=CARTESIAN_POINT('Origin',(-21.8945024061954,373.533891528942,120.000000000001));
#5443=CARTESIAN_POINT('',(-11.8945024061954,373.533891528942,120.000000000001));
#5444=CARTESIAN_POINT('Origin',(21.8945024061954,373.533891528942,120.000000000001));
#5445=CARTESIAN_POINT('',(31.8945024061955,373.533891528942,120.000000000001));
#5446=CARTESIAN_POINT('Origin',(21.8945024061954,373.533891528942,120.000000000001));
#5447=CARTESIAN_POINT('',(31.8945024061955,373.533891528942,120.000000000001));
#5448=CARTESIAN_POINT('Origin',(-21.8945024061954,333.533891528942,120.000000000001));
#5449=CARTESIAN_POINT('',(-11.8945024061954,333.533891528942,120.000000000001));
#5450=CARTESIAN_POINT('Origin',(-21.8945024061954,333.533891528942,120.000000000001));
#5451=CARTESIAN_POINT('',(-11.8945024061954,333.533891528942,120.000000000001));
#5452=CARTESIAN_POINT('Origin',(21.8945024061954,333.533891528942,120.000000000001));
#5453=CARTESIAN_POINT('',(31.8945024061955,333.533891528942,120.000000000001));
#5454=CARTESIAN_POINT('Origin',(21.8945024061954,333.533891528942,120.000000000001));
#5455=CARTESIAN_POINT('',(31.8945024061955,333.533891528942,120.000000000001));
#5456=CARTESIAN_POINT('Origin',(-67.5061608111161,485.5,105.000000000001));
#5457=CARTESIAN_POINT('',(-67.5061608111161,460.5,85.0000000000015));
#5458=CARTESIAN_POINT('',(-67.5061608111161,460.5,98.7500000000015));
#5459=CARTESIAN_POINT('',(-67.5061608111161,245.5,85.0000000000015));
#5460=CARTESIAN_POINT('',(-67.5061608111161,245.5,105.000000000001));
#5461=CARTESIAN_POINT('',(-67.5061608111161,485.5,85.0000000000015));
#5462=CARTESIAN_POINT('Origin',(-67.5061608111161,485.5,85.0000000000015));
#5463=CARTESIAN_POINT('',(-51.5061608111161,460.5,85.0000000000015));
#5464=CARTESIAN_POINT('',(-54.3796206083371,460.5,85.0000000000015));
#5465=CARTESIAN_POINT('',(-51.5061608111161,245.5,85.0000000000015));
#5466=CARTESIAN_POINT('',(-67.5061608111161,245.5,85.0000000000015));
#5467=CARTESIAN_POINT('',(-51.5061608111161,485.5,85.0000000000015));
#5468=CARTESIAN_POINT('Origin',(-51.5061608111161,485.5,85.0000000000015));
#5469=CARTESIAN_POINT('',(-51.5061608111161,460.5,65.0000000000015));
#5470=CARTESIAN_POINT('',(-51.5061608111161,460.5,88.7500000000015));
#5471=CARTESIAN_POINT('',(-51.5061608111161,245.5,65.0000000000015));
#5472=CARTESIAN_POINT('',(-51.5061608111161,245.5,85.0000000000015));
#5473=CARTESIAN_POINT('',(-51.5061608111161,485.5,65.0000000000015));
#5474=CARTESIAN_POINT('Origin',(-82.5061608111161,485.5,65.0000000000015));
#5475=CARTESIAN_POINT('',(-82.5061608111161,460.5,65.0000000000015));
#5476=CARTESIAN_POINT('',(-82.5061608111161,460.5,120.000000000001));
#5477=CARTESIAN_POINT('',(-82.5061608111161,460.5,78.7500000000015));
#5478=CARTESIAN_POINT('',(-82.5061608111161,245.5,65.0000000000015));
#5479=CARTESIAN_POINT('',(-82.5061608111161,485.5,65.0000000000015));
#5480=CARTESIAN_POINT('',(-82.5061608111161,245.5,120.000000000001));
#5481=CARTESIAN_POINT('',(-82.5061608111161,245.5,20.0000000000015));
#5482=CARTESIAN_POINT('',(-82.5061608111161,485.5,120.000000000001));
#5483=CARTESIAN_POINT('Origin',(-51.5061608111161,485.5,65.0000000000015));
#5484=CARTESIAN_POINT('',(-46.3796206083371,460.5,65.0000000000015));
#5485=CARTESIAN_POINT('',(-51.5061608111161,245.5,65.0000000000015));
#5486=CARTESIAN_POINT('Origin',(41.2530804055581,460.5,92.5000000000015));
#5487=CARTESIAN_POINT('',(51.5061608111161,460.5,85.0000000000015));
#5488=CARTESIAN_POINT('',(51.5061608111161,460.5,65.0000000000015));
#5489=CARTESIAN_POINT('',(51.5061608111161,460.5,88.7500000000015));
#5490=CARTESIAN_POINT('',(67.5061608111161,460.5,85.0000000000015));
#5491=CARTESIAN_POINT('',(54.3796206083371,460.5,85.0000000000015));
#5492=CARTESIAN_POINT('',(67.5061608111161,460.5,98.7500000000015));
#5493=CARTESIAN_POINT('',(82.5061608111161,460.5,120.000000000001));
#5494=CARTESIAN_POINT('',(-61.8796206083371,460.5,120.000000000001));
#5495=CARTESIAN_POINT('',(82.5061608111161,460.5,65.0000000000015));
#5496=CARTESIAN_POINT('',(82.5061608111161,460.5,78.7500000000015));
#5497=CARTESIAN_POINT('',(46.3796206083371,460.5,65.0000000000015));
#5498=CARTESIAN_POINT('Origin',(67.5061608111161,485.5,105.000000000001));
#5499=CARTESIAN_POINT('',(67.5061608111161,245.5,85.0000000000015));
#5500=CARTESIAN_POINT('',(67.5061608111161,485.5,85.0000000000015));
#5501=CARTESIAN_POINT('',(67.5061608111161,245.5,105.000000000001));
#5502=CARTESIAN_POINT('Origin',(67.5061608111161,485.5,85.0000000000015));
#5503=CARTESIAN_POINT('',(51.5061608111161,245.5,85.0000000000015));
#5504=CARTESIAN_POINT('',(51.5061608111161,485.5,85.0000000000015));
#5505=CARTESIAN_POINT('',(67.5061608111161,245.5,85.0000000000015));
#5506=CARTESIAN_POINT('Origin',(51.5061608111161,485.5,85.0000000000015));
#5507=CARTESIAN_POINT('',(51.5061608111161,245.5,65.0000000000015));
#5508=CARTESIAN_POINT('',(51.5061608111161,485.5,65.0000000000015));
#5509=CARTESIAN_POINT('',(51.5061608111161,245.5,85.0000000000015));
#5510=CARTESIAN_POINT('Origin',(82.5061608111161,485.5,120.000000000001));
#5511=CARTESIAN_POINT('',(82.5061608111161,245.5,120.000000000001));
#5512=CARTESIAN_POINT('',(82.5061608111161,245.5,120.000000000001));
#5513=CARTESIAN_POINT('',(82.5061608111161,485.5,120.000000000001));
#5514=CARTESIAN_POINT('Origin',(82.5061608111161,485.5,65.0000000000015));
#5515=CARTESIAN_POINT('',(82.5061608111161,245.5,65.0000000000015));
#5516=CARTESIAN_POINT('',(82.5061608111161,245.5,20.0000000000015));
#5517=CARTESIAN_POINT('',(82.5061608111161,485.5,65.0000000000015));
#5518=CARTESIAN_POINT('Origin',(51.5061608111161,485.5,65.0000000000015));
#5519=CARTESIAN_POINT('',(51.5061608111161,245.5,65.0000000000015));
#5520=CARTESIAN_POINT('Origin',(41.2530804055581,245.5,92.5000000000015));
#6074=UNCERTAINTY_MEASURE_WITH_UNIT(LENGTH_MEASURE(0.01),#6097,
'DISTANCE_ACCURACY_VALUE',
'Maximum model space distance between geometric entities at asserted c
onnectivities');
#6083=UNCERTAINTY_MEASURE_WITH_UNIT(LENGTH_MEASURE(0.01),#6097,
'DISTANCE_ACCURACY_VALUE',
'Maximum model space distance between geometric entities at asserted c
onnectivities');
#6087=(
GEOMETRIC_REPRESENTATION_CONTEXT(3)
GLOBAL_UNCERTAINTY_ASSIGNED_CONTEXT((#6074))
GLOBAL_UNIT_ASSIGNED_CONTEXT((#6097,#6099,#6100))
REPRESENTATION_CONTEXT('','3D')
);
#6096=(
GEOMETRIC_REPRESENTATION_CONTEXT(3)
GLOBAL_UNCERTAINTY_ASSIGNED_CONTEXT((#6083))
GLOBAL_UNIT_ASSIGNED_CONTEXT((#6097,#6099,#6100))
REPRESENTATION_CONTEXT('','3D')
);
#6097=(
LENGTH_UNIT()
NAMED_UNIT(*)
SI_UNIT(.MILLI.,.METRE.)
);
#6099=(
NAMED_UNIT(*)
PLANE_ANGLE_UNIT()
SI_UNIT($,.RADIAN.)
);
#6100=(
NAMED_UNIT(*)
SI_UNIT($,.STERADIAN.)
SOLID_ANGLE_UNIT()
);
#6104=SHAPE_DEFINITION_REPRESENTATION(#6116,#6139);
#6116=PRODUCT_DEFINITION_SHAPE('',$,#6152);
#6139=SHAPE_REPRESENTATION('',(#3806),#6087);
#6148=PRODUCT_DEFINITION_CONTEXT('part definition',#6186,'design');
#6152=PRODUCT_DEFINITION('Plate','Plate',#6164,#6148);
#6164=PRODUCT_DEFINITION_FORMATION('',$,#6191);
#6186=APPLICATION_CONTEXT(
'Core Data for Automotive Mechanical Design Process');
#6187=PRODUCT_CONTEXT('part definition',#6186,'mechanical');
#6191=PRODUCT('Plate','Plate',$,(#6187));
#6263=COLOUR_RGB('Off White',0.89,0.88,0.83);
#6264=FILL_AREA_STYLE_COLOUR('',#6263);
#6265=FILL_AREA_STYLE('',(#6264));
#6266=SURFACE_STYLE_FILL_AREA(#6265);
#6267=SURFACE_SIDE_STYLE('',(#6266));
#6268=SURFACE_STYLE_USAGE(.BOTH.,#6267);
#6269=PRESENTATION_STYLE_ASSIGNMENT((#6268));
ENDSEC;
END-ISO-10303-21;
